ISO-10303-21;
HEADER;
/* Generated by software containing ST-Developer
 * from STEP Tools, Inc. (www.steptools.com) 
 */

FILE_DESCRIPTION(
/* description */ ('Hand wheel with handle and shaft collar'),
/* implementation_level */ '2;1');

FILE_NAME(
/* name */ 'M6x18 mounting screw.step',
/* time_stamp */ '2026-10-28T03:23:19-07:00',
/* author */ (''),
/* organization */ (''),
/* preprocessor_version */ 'ST-DEVELOPER v20.2',
/* originating_system */ 'Autodesk Translation Framework v15.17.0.0',
/* authorisation */ '');

FILE_SCHEMA (('AUTOMOTIVE_DESIGN { 1 0 10303 214 3 1 1 }'));
ENDSEC;

DATA;
#10=MECHANICAL_DESIGN_GEOMETRIC_PRESENTATION_REPRESENTATION('',(#403),#10510);
#301=CONICAL_SURFACE('',#5851,0.475,0.785398163397449);
#302=CONICAL_SURFACE('',#5855,0.485,0.785398163397448);
#303=CONICAL_SURFACE('',#5859,0.31,0.463647609000806);
#325=ORIENTED_CLOSED_SHELL('',*,#5302,.F.);
#328=BREP_WITH_VOIDS('Body1',#5303,(#325));
#339=SHAPE_REPRESENTATION_RELATIONSHIP('SRR','None',#10655,#371);
#371=ADVANCED_BREP_SHAPE_REPRESENTATION('',(#328),#10482);
#403=STYLED_ITEM('',(#10915),#328);
#538=FACE_BOUND('',#1217,.T.);
#636=PLANE('',#5839);
#637=PLANE('',#5840);
#638=PLANE('',#5841);
#639=PLANE('',#5842);
#640=PLANE('',#5843);
#641=PLANE('',#5844);
#642=PLANE('',#5845);
#643=PLANE('',#5846);
#644=PLANE('',#5847);
#645=PLANE('',#5849);
#646=PLANE('',#5857);
#832=FACE_OUTER_BOUND('',#1203,.T.);
#833=FACE_OUTER_BOUND('',#1204,.T.);
#834=FACE_OUTER_BOUND('',#1205,.T.);
#835=FACE_OUTER_BOUND('',#1206,.T.);
#836=FACE_OUTER_BOUND('',#1207,.T.);
#837=FACE_OUTER_BOUND('',#1208,.T.);
#838=FACE_OUTER_BOUND('',#1209,.T.);
#839=FACE_OUTER_BOUND('',#1210,.T.);
#840=FACE_OUTER_BOUND('',#1211,.T.);
#841=FACE_OUTER_BOUND('',#1212,.T.);
#842=FACE_OUTER_BOUND('',#1213,.T.);
#843=FACE_OUTER_BOUND('',#1214,.T.);
#844=FACE_OUTER_BOUND('',#1215,.T.);
#845=FACE_OUTER_BOUND('',#1216,.T.);
#846=FACE_OUTER_BOUND('',#1218,.T.);
#847=FACE_OUTER_BOUND('',#1219,.T.);
#1203=EDGE_LOOP('',(#3863,#3864,#3865,#3866));
#1204=EDGE_LOOP('',(#3867,#3868,#3869,#3870));
#1205=EDGE_LOOP('',(#3871,#3872,#3873,#3874));
#1206=EDGE_LOOP('',(#3875,#3876,#3877,#3878));
#1207=EDGE_LOOP('',(#3879,#3880,#3881,#3882));
#1208=EDGE_LOOP('',(#3883,#3884,#3885,#3886));
#1209=EDGE_LOOP('',(#3887,#3888,#3889,#3890,#3891,#3892));
#1210=EDGE_LOOP('',(#3893,#3894,#3895,#3896,#3897,#3898));
#1211=EDGE_LOOP('',(#3899));
#1212=EDGE_LOOP('',(#3900));
#1213=EDGE_LOOP('',(#3901,#3902,#3903,#3904));
#1214=EDGE_LOOP('',(#3905,#3906,#3907,#3908));
#1215=EDGE_LOOP('',(#3909,#3910,#3911,#3912));
#1216=EDGE_LOOP('',(#3913));
#1217=EDGE_LOOP('',(#3914));
#1218=EDGE_LOOP('',(#3915,#3916,#3917,#3918));
#1219=EDGE_LOOP('',(#3919,#3920,#3921,#3922));
#1604=LINE('',#8511,#1914);
#1605=LINE('',#8513,#1915);
#1606=LINE('',#8515,#1916);
#1607=LINE('',#8516,#1917);
#1608=LINE('',#8519,#1918);
#1609=LINE('',#8521,#1919);
#1610=LINE('',#8522,#1920);
#1611=LINE('',#8525,#1921);
#1612=LINE('',#8527,#1922);
#1613=LINE('',#8528,#1923);
#1614=LINE('',#8531,#1924);
#1615=LINE('',#8533,#1925);
#1616=LINE('',#8534,#1926);
#1617=LINE('',#8537,#1927);
#1618=LINE('',#8539,#1928);
#1619=LINE('',#8540,#1929);
#1620=LINE('',#8542,#1930);
#1621=LINE('',#8543,#1931);
#1622=LINE('',#8555,#1932);
#1623=LINE('',#8559,#1933);
#1624=LINE('',#8563,#1934);
#1625=LINE('',#8570,#1935);
#1626=LINE('',#8572,#1936);
#1914=VECTOR('',#6796,1.);
#1915=VECTOR('',#6797,1.);
#1916=VECTOR('',#6798,1.);
#1917=VECTOR('',#6799,1.);
#1918=VECTOR('',#6802,1.);
#1919=VECTOR('',#6803,1.);
#1920=VECTOR('',#6804,1.);
#1921=VECTOR('',#6807,1.);
#1922=VECTOR('',#6808,1.);
#1923=VECTOR('',#6809,1.);
#1924=VECTOR('',#6812,1.);
#1925=VECTOR('',#6813,1.);
#1926=VECTOR('',#6814,1.);
#1927=VECTOR('',#6817,1.);
#1928=VECTOR('',#6818,1.);
#1929=VECTOR('',#6819,1.);
#1930=VECTOR('',#6822,1.);
#1931=VECTOR('',#6823,1.);
#1932=VECTOR('',#6840,0.475);
#1933=VECTOR('',#6845,0.5);
#1934=VECTOR('',#6850,0.485);
#1935=VECTOR('',#6859,0.31);
#1936=VECTOR('',#6862,0.3);
#2195=CIRCLE('',#5848,0.2942);
#2196=CIRCLE('',#5850,0.45);
#2197=CIRCLE('',#5852,0.5);
#2198=CIRCLE('',#5854,0.5);
#2199=CIRCLE('',#5856,0.47);
#2200=CIRCLE('',#5858,0.32);
#2201=CIRCLE('',#5860,0.2942);
#2546=VERTEX_POINT('',#8509);
#2547=VERTEX_POINT('',#8510);
#2548=VERTEX_POINT('',#8512);
#2549=VERTEX_POINT('',#8514);
#2550=VERTEX_POINT('',#8518);
#2551=VERTEX_POINT('',#8520);
#2552=VERTEX_POINT('',#8524);
#2553=VERTEX_POINT('',#8526);
#2554=VERTEX_POINT('',#8530);
#2555=VERTEX_POINT('',#8532);
#2556=VERTEX_POINT('',#8536);
#2557=VERTEX_POINT('',#8538);
#2558=VERTEX_POINT('',#8547);
#2559=VERTEX_POINT('',#8550);
#2560=VERTEX_POINT('',#8553);
#2561=VERTEX_POINT('',#8557);
#2562=VERTEX_POINT('',#8561);
#2563=VERTEX_POINT('',#8565);
#2564=VERTEX_POINT('',#8568);
#3049=EDGE_CURVE('',#2546,#2547,#1604,.T.);
#3050=EDGE_CURVE('',#2547,#2548,#1605,.T.);
#3051=EDGE_CURVE('',#2548,#2549,#1606,.T.);
#3052=EDGE_CURVE('',#2546,#2549,#1607,.T.);
#3053=EDGE_CURVE('',#2547,#2550,#1608,.T.);
#3054=EDGE_CURVE('',#2550,#2551,#1609,.T.);
#3055=EDGE_CURVE('',#2551,#2548,#1610,.T.);
#3056=EDGE_CURVE('',#2550,#2552,#1611,.T.);
#3057=EDGE_CURVE('',#2552,#2553,#1612,.T.);
#3058=EDGE_CURVE('',#2553,#2551,#1613,.T.);
#3059=EDGE_CURVE('',#2552,#2554,#1614,.T.);
#3060=EDGE_CURVE('',#2554,#2555,#1615,.T.);
#3061=EDGE_CURVE('',#2555,#2553,#1616,.T.);
#3062=EDGE_CURVE('',#2554,#2556,#1617,.T.);
#3063=EDGE_CURVE('',#2556,#2557,#1618,.T.);
#3064=EDGE_CURVE('',#2557,#2555,#1619,.T.);
#3065=EDGE_CURVE('',#2556,#2546,#1620,.T.);
#3066=EDGE_CURVE('',#2549,#2557,#1621,.T.);
#3067=EDGE_CURVE('',#2558,#2558,#2195,.T.);
#3068=EDGE_CURVE('',#2559,#2559,#2196,.T.);
#3069=EDGE_CURVE('',#2560,#2560,#2197,.T.);
#3070=EDGE_CURVE('',#2560,#2559,#1622,.T.);
#3071=EDGE_CURVE('',#2561,#2561,#2198,.T.);
#3072=EDGE_CURVE('',#2561,#2560,#1623,.T.);
#3073=EDGE_CURVE('',#2562,#2562,#2199,.T.);
#3074=EDGE_CURVE('',#2562,#2561,#1624,.T.);
#3075=EDGE_CURVE('',#2563,#2563,#2200,.T.);
#3076=EDGE_CURVE('',#2564,#2564,#2201,.F.);
#3077=EDGE_CURVE('',#2564,#2563,#1625,.T.);
#3078=EDGE_CURVE('',#2558,#2564,#1626,.T.);
#3863=ORIENTED_EDGE('',*,*,#3049,.T.);
#3864=ORIENTED_EDGE('',*,*,#3050,.T.);
#3865=ORIENTED_EDGE('',*,*,#3051,.T.);
#3866=ORIENTED_EDGE('',*,*,#3052,.F.);
#3867=ORIENTED_EDGE('',*,*,#3053,.T.);
#3868=ORIENTED_EDGE('',*,*,#3054,.T.);
#3869=ORIENTED_EDGE('',*,*,#3055,.T.);
#3870=ORIENTED_EDGE('',*,*,#3050,.F.);
#3871=ORIENTED_EDGE('',*,*,#3056,.T.);
#3872=ORIENTED_EDGE('',*,*,#3057,.T.);
#3873=ORIENTED_EDGE('',*,*,#3058,.T.);
#3874=ORIENTED_EDGE('',*,*,#3054,.F.);
#3875=ORIENTED_EDGE('',*,*,#3059,.T.);
#3876=ORIENTED_EDGE('',*,*,#3060,.T.);
#3877=ORIENTED_EDGE('',*,*,#3061,.T.);
#3878=ORIENTED_EDGE('',*,*,#3057,.F.);
#3879=ORIENTED_EDGE('',*,*,#3062,.T.);
#3880=ORIENTED_EDGE('',*,*,#3063,.T.);
#3881=ORIENTED_EDGE('',*,*,#3064,.T.);
#3882=ORIENTED_EDGE('',*,*,#3060,.F.);
#3883=ORIENTED_EDGE('',*,*,#3065,.T.);
#3884=ORIENTED_EDGE('',*,*,#3052,.T.);
#3885=ORIENTED_EDGE('',*,*,#3066,.T.);
#3886=ORIENTED_EDGE('',*,*,#3063,.F.);
#3887=ORIENTED_EDGE('',*,*,#3065,.F.);
#3888=ORIENTED_EDGE('',*,*,#3062,.F.);
#3889=ORIENTED_EDGE('',*,*,#3059,.F.);
#3890=ORIENTED_EDGE('',*,*,#3056,.F.);
#3891=ORIENTED_EDGE('',*,*,#3053,.F.);
#3892=ORIENTED_EDGE('',*,*,#3049,.F.);
#3893=ORIENTED_EDGE('',*,*,#3066,.F.);
#3894=ORIENTED_EDGE('',*,*,#3051,.F.);
#3895=ORIENTED_EDGE('',*,*,#3055,.F.);
#3896=ORIENTED_EDGE('',*,*,#3058,.F.);
#3897=ORIENTED_EDGE('',*,*,#3061,.F.);
#3898=ORIENTED_EDGE('',*,*,#3064,.F.);
#3899=ORIENTED_EDGE('',*,*,#3067,.F.);
#3900=ORIENTED_EDGE('',*,*,#3068,.F.);
#3901=ORIENTED_EDGE('',*,*,#3069,.F.);
#3902=ORIENTED_EDGE('',*,*,#3070,.T.);
#3903=ORIENTED_EDGE('',*,*,#3068,.T.);
#3904=ORIENTED_EDGE('',*,*,#3070,.F.);
#3905=ORIENTED_EDGE('',*,*,#3071,.F.);
#3906=ORIENTED_EDGE('',*,*,#3072,.T.);
#3907=ORIENTED_EDGE('',*,*,#3069,.T.);
#3908=ORIENTED_EDGE('',*,*,#3072,.F.);
#3909=ORIENTED_EDGE('',*,*,#3073,.F.);
#3910=ORIENTED_EDGE('',*,*,#3074,.T.);
#3911=ORIENTED_EDGE('',*,*,#3071,.T.);
#3912=ORIENTED_EDGE('',*,*,#3074,.F.);
#3913=ORIENTED_EDGE('',*,*,#3073,.T.);
#3914=ORIENTED_EDGE('',*,*,#3075,.F.);
#3915=ORIENTED_EDGE('',*,*,#3076,.F.);
#3916=ORIENTED_EDGE('',*,*,#3077,.T.);
#3917=ORIENTED_EDGE('',*,*,#3075,.T.);
#3918=ORIENTED_EDGE('',*,*,#3077,.F.);
#3919=ORIENTED_EDGE('',*,*,#3067,.T.);
#3920=ORIENTED_EDGE('',*,*,#3078,.T.);
#3921=ORIENTED_EDGE('',*,*,#3076,.T.);
#3922=ORIENTED_EDGE('',*,*,#3078,.F.);
#4910=CYLINDRICAL_SURFACE('',#5853,0.5);
#4911=CYLINDRICAL_SURFACE('',#5861,0.2942);
#5044=ADVANCED_FACE('',(#832),#636,.F.);
#5045=ADVANCED_FACE('',(#833),#637,.F.);
#5046=ADVANCED_FACE('',(#834),#638,.F.);
#5047=ADVANCED_FACE('',(#835),#639,.F.);
#5048=ADVANCED_FACE('',(#836),#640,.F.);
#5049=ADVANCED_FACE('',(#837),#641,.F.);
#5050=ADVANCED_FACE('',(#838),#642,.F.);
#5051=ADVANCED_FACE('',(#839),#643,.F.);
#5052=ADVANCED_FACE('',(#840),#644,.F.);
#5053=ADVANCED_FACE('',(#841),#645,.T.);
#5054=ADVANCED_FACE('',(#842),#301,.T.);
#5055=ADVANCED_FACE('',(#843),#4910,.T.);
#5056=ADVANCED_FACE('',(#844),#302,.T.);
#5057=ADVANCED_FACE('',(#845,#538),#646,.T.);
#5058=ADVANCED_FACE('',(#846),#303,.T.);
#5059=ADVANCED_FACE('',(#847),#4911,.T.);
#5302=CLOSED_SHELL('',(#5044,#5045,#5046,#5047,#5048,#5049,#5050,#5051));
#5303=CLOSED_SHELL('',(#5052,#5053,#5054,#5055,#5056,#5057,#5058,#5059));
#5838=AXIS2_PLACEMENT_3D('',#8507,#6792,#6793);
#5839=AXIS2_PLACEMENT_3D('',#8508,#6794,#6795);
#5840=AXIS2_PLACEMENT_3D('',#8517,#6800,#6801);
#5841=AXIS2_PLACEMENT_3D('',#8523,#6805,#6806);
#5842=AXIS2_PLACEMENT_3D('',#8529,#6810,#6811);
#5843=AXIS2_PLACEMENT_3D('',#8535,#6815,#6816);
#5844=AXIS2_PLACEMENT_3D('',#8541,#6820,#6821);
#5845=AXIS2_PLACEMENT_3D('',#8544,#6824,#6825);
#5846=AXIS2_PLACEMENT_3D('',#8545,#6826,#6827);
#5847=AXIS2_PLACEMENT_3D('',#8546,#6828,#6829);
#5848=AXIS2_PLACEMENT_3D('',#8548,#6830,#6831);
#5849=AXIS2_PLACEMENT_3D('',#8549,#6832,#6833);
#5850=AXIS2_PLACEMENT_3D('',#8551,#6834,#6835);
#5851=AXIS2_PLACEMENT_3D('',#8552,#6836,#6837);
#5852=AXIS2_PLACEMENT_3D('',#8554,#6838,#6839);
#5853=AXIS2_PLACEMENT_3D('',#8556,#6841,#6842);
#5854=AXIS2_PLACEMENT_3D('',#8558,#6843,#6844);
#5855=AXIS2_PLACEMENT_3D('',#8560,#6846,#6847);
#5856=AXIS2_PLACEMENT_3D('',#8562,#6848,#6849);
#5857=AXIS2_PLACEMENT_3D('',#8564,#6851,#6852);
#5858=AXIS2_PLACEMENT_3D('',#8566,#6853,#6854);
#5859=AXIS2_PLACEMENT_3D('',#8567,#6855,#6856);
#5860=AXIS2_PLACEMENT_3D('',#8569,#6857,#6858);
#5861=AXIS2_PLACEMENT_3D('',#8571,#6860,#6861);
#6792=DIRECTION('axis',(0.,0.,1.));
#6793=DIRECTION('refdir',(1.,0.,0.));
#6794=DIRECTION('center_axis',(0.866025403784439,0.,-0.5));
#6795=DIRECTION('ref_axis',(0.5,0.,0.866025403784439));
#6796=DIRECTION('',(-0.5,0.,-0.866025403784439));
#6797=DIRECTION('',(0.,-1.,0.));
#6798=DIRECTION('',(0.5,0.,0.866025403784439));
#6799=DIRECTION('',(0.,-1.,0.));
#6800=DIRECTION('center_axis',(1.92296268638356E-16,0.,-1.));
#6801=DIRECTION('ref_axis',(1.,0.,1.92296268638356E-16));
#6802=DIRECTION('',(-1.,0.,-1.92296268638356E-16));
#6803=DIRECTION('',(0.,-1.,0.));
#6804=DIRECTION('',(1.,0.,1.92296268638356E-16));
#6805=DIRECTION('center_axis',(-0.866025403784439,0.,-0.5));
#6806=DIRECTION('ref_axis',(0.5,0.,-0.866025403784439));
#6807=DIRECTION('',(-0.5,0.,0.866025403784438));
#6808=DIRECTION('',(0.,-1.,0.));
#6809=DIRECTION('',(0.5,0.,-0.866025403784438));
#6810=DIRECTION('center_axis',(-0.866025403784439,0.,0.5));
#6811=DIRECTION('ref_axis',(-0.5,0.,-0.866025403784439));
#6812=DIRECTION('',(0.5,0.,0.866025403784439));
#6813=DIRECTION('',(0.,-1.,0.));
#6814=DIRECTION('',(-0.5,0.,-0.866025403784439));
#6815=DIRECTION('center_axis',(-1.92296268638356E-16,0.,1.));
#6816=DIRECTION('ref_axis',(-1.,0.,-1.92296268638356E-16));
#6817=DIRECTION('',(1.,0.,1.92296268638356E-16));
#6818=DIRECTION('',(0.,-1.,0.));
#6819=DIRECTION('',(-1.,0.,-1.92296268638356E-16));
#6820=DIRECTION('center_axis',(0.866025403784439,0.,0.5));
#6821=DIRECTION('ref_axis',(-0.5,0.,0.866025403784439));
#6822=DIRECTION('',(0.5,0.,-0.866025403784439));
#6823=DIRECTION('',(-0.5,0.,0.866025403784439));
#6824=DIRECTION('center_axis',(0.,1.,0.));
#6825=DIRECTION('ref_axis',(1.,0.,0.));
#6826=DIRECTION('center_axis',(0.,-1.,0.));
#6827=DIRECTION('ref_axis',(0.,0.,-1.));
#6828=DIRECTION('center_axis',(0.,1.,0.));
#6829=DIRECTION('ref_axis',(1.,0.,0.));
#6830=DIRECTION('center_axis',(0.,1.,0.));
#6831=DIRECTION('ref_axis',(1.,0.,0.));
#6832=DIRECTION('center_axis',(0.,1.,0.));
#6833=DIRECTION('ref_axis',(0.,0.,1.));
#6834=DIRECTION('center_axis',(0.,-1.,0.));
#6835=DIRECTION('ref_axis',(1.,0.,0.));
#6836=DIRECTION('center_axis',(0.,-1.,0.));
#6837=DIRECTION('ref_axis',(1.,0.,0.));
#6838=DIRECTION('center_axis',(0.,-1.,0.));
#6839=DIRECTION('ref_axis',(1.,0.,0.));
#6840=DIRECTION('',(0.707106781186548,0.707106781186547,8.65956056235494E-17));
#6841=DIRECTION('center_axis',(0.,-1.,0.));
#6842=DIRECTION('ref_axis',(1.,0.,0.));
#6843=DIRECTION('center_axis',(0.,-1.,0.));
#6844=DIRECTION('ref_axis',(1.,0.,0.));
#6845=DIRECTION('',(0.,1.,0.));
#6846=DIRECTION('center_axis',(0.,1.,0.));
#6847=DIRECTION('ref_axis',(1.,0.,0.));
#6848=DIRECTION('center_axis',(0.,-1.,0.));
#6849=DIRECTION('ref_axis',(1.,0.,0.));
#6850=DIRECTION('',(-0.707106781186547,0.707106781186548,-8.65956056235493E-17));
#6851=DIRECTION('center_axis',(0.,-1.,0.));
#6852=DIRECTION('ref_axis',(0.,0.,-1.));
#6853=DIRECTION('center_axis',(0.,-1.,0.));
#6854=DIRECTION('ref_axis',(1.,0.,0.));
#6855=DIRECTION('center_axis',(0.,1.,0.));
#6856=DIRECTION('ref_axis',(1.,0.,0.));
#6857=DIRECTION('center_axis',(0.,1.,0.));
#6858=DIRECTION('ref_axis',(1.,0.,0.));
#6859=DIRECTION('',(-0.447213595499958,0.894427190999916,-5.47678698264203E-17));
#6860=DIRECTION('center_axis',(0.,-1.,0.));
#6861=DIRECTION('ref_axis',(1.,0.,0.));
#6862=DIRECTION('',(0.,1.,0.));
#8507=CARTESIAN_POINT('',(0.,0.,0.));
#8508=CARTESIAN_POINT('Origin',(0.144337567297406,-0.6,-0.25));
#8509=CARTESIAN_POINT('',(0.288675134594813,-0.6,0.));
#8510=CARTESIAN_POINT('',(0.144337567297406,-0.6,-0.25));
#8511=CARTESIAN_POINT('',(0.288675134594813,-0.6,0.));
#8512=CARTESIAN_POINT('',(0.144337567297406,-0.96,-0.25));
#8513=CARTESIAN_POINT('',(0.144337567297406,-0.6,-0.25));
#8514=CARTESIAN_POINT('',(0.288675134594813,-0.96,0.));
#8515=CARTESIAN_POINT('',(0.288675134594813,-0.96,0.));
#8516=CARTESIAN_POINT('',(0.288675134594813,-0.6,0.));
#8517=CARTESIAN_POINT('Origin',(-0.144337567297406,-0.6,-0.25));
#8518=CARTESIAN_POINT('',(-0.144337567297406,-0.6,-0.25));
#8519=CARTESIAN_POINT('',(0.144337567297406,-0.6,-0.25));
#8520=CARTESIAN_POINT('',(-0.144337567297406,-0.96,-0.25));
#8521=CARTESIAN_POINT('',(-0.144337567297406,-0.6,-0.25));
#8522=CARTESIAN_POINT('',(0.144337567297406,-0.96,-0.25));
#8523=CARTESIAN_POINT('Origin',(-0.288675134594813,-0.6,-8.32667268468867E-17));
#8524=CARTESIAN_POINT('',(-0.288675134594813,-0.6,-3.53525079574969E-17));
#8525=CARTESIAN_POINT('',(-0.144337567297406,-0.6,-0.25));
#8526=CARTESIAN_POINT('',(-0.288675134594813,-0.96,-5.55111512312578E-17));
#8527=CARTESIAN_POINT('',(-0.288675134594813,-0.6,-3.53525079574969E-17));
#8528=CARTESIAN_POINT('',(-0.144337567297406,-0.96,-0.25));
#8529=CARTESIAN_POINT('Origin',(-0.144337567297407,-0.6,0.25));
#8530=CARTESIAN_POINT('',(-0.144337567297407,-0.6,0.25));
#8531=CARTESIAN_POINT('',(-0.288675134594813,-0.6,-3.53525079574969E-17));
#8532=CARTESIAN_POINT('',(-0.144337567297407,-0.96,0.25));
#8533=CARTESIAN_POINT('',(-0.144337567297407,-0.6,0.25));
#8534=CARTESIAN_POINT('',(-0.288675134594813,-0.96,-3.53525079574969E-17));
#8535=CARTESIAN_POINT('Origin',(0.144337567297406,-0.6,0.25));
#8536=CARTESIAN_POINT('',(0.144337567297406,-0.6,0.25));
#8537=CARTESIAN_POINT('',(-0.144337567297407,-0.6,0.25));
#8538=CARTESIAN_POINT('',(0.144337567297406,-0.96,0.25));
#8539=CARTESIAN_POINT('',(0.144337567297406,-0.6,0.25));
#8540=CARTESIAN_POINT('',(-0.144337567297407,-0.96,0.25));
#8541=CARTESIAN_POINT('Origin',(0.288675134594813,-0.6,0.));
#8542=CARTESIAN_POINT('',(0.144337567297406,-0.6,0.25));
#8543=CARTESIAN_POINT('',(0.144337567297406,-0.96,0.25));
#8544=CARTESIAN_POINT('Origin',(0.,-0.6,0.));
#8545=CARTESIAN_POINT('Origin',(0.,-0.96,0.));
#8546=CARTESIAN_POINT('Origin',(0.,-1.8,0.));
#8547=CARTESIAN_POINT('',(-0.2942,-1.8,3.60291088309151E-17));
#8548=CARTESIAN_POINT('Origin',(0.,-1.8,0.));
#8549=CARTESIAN_POINT('Origin',(0.45,0.6,0.));
#8550=CARTESIAN_POINT('',(-0.45,0.6,-5.51091059616309E-17));
#8551=CARTESIAN_POINT('Origin',(0.,0.6,0.));
#8552=CARTESIAN_POINT('Origin',(0.,0.575,0.));
#8553=CARTESIAN_POINT('',(-0.5,0.55,-6.12323399573677E-17));
#8554=CARTESIAN_POINT('Origin',(0.,0.55,0.));
#8555=CARTESIAN_POINT('',(-0.475,0.575,-5.81707229594993E-17));
#8556=CARTESIAN_POINT('Origin',(0.,0.29,0.));
#8557=CARTESIAN_POINT('',(-0.5,0.0299999999999998,-6.12323399573677E-17));
#8558=CARTESIAN_POINT('Origin',(0.,0.0299999999999998,0.));
#8559=CARTESIAN_POINT('',(-0.5,0.29,-6.12323399573677E-17));
#8560=CARTESIAN_POINT('Origin',(0.,0.0150000000000001,0.));
#8561=CARTESIAN_POINT('',(-0.47,7.11236625150491E-17,-5.75583995599256E-17));
#8562=CARTESIAN_POINT('Origin',(0.,0.,0.));
#8563=CARTESIAN_POINT('',(-0.485,0.0150000000000001,-5.93953697586466E-17));
#8564=CARTESIAN_POINT('Origin',(0.32,0.,0.));
#8565=CARTESIAN_POINT('',(-0.32,-6.93889390390723E-18,-3.91886975727153E-17));
#8566=CARTESIAN_POINT('Origin',(0.,0.,0.));
#8567=CARTESIAN_POINT('Origin',(0.,-0.02,0.));
#8568=CARTESIAN_POINT('',(-0.2942,-0.0515999999999999,3.60291088309151E-17));
#8569=CARTESIAN_POINT('Origin',(0.,-0.0515999999999999,0.));
#8570=CARTESIAN_POINT('',(-0.31,-0.02,-3.7964050773568E-17));
#8571=CARTESIAN_POINT('Origin',(0.,-1.24,0.));
#8572=CARTESIAN_POINT('',(-0.2942,-1.24,-3.60291088309151E-17));
#10443=UNCERTAINTY_MEASURE_WITH_UNIT(LENGTH_MEASURE(0.001),#10511,
'DISTANCE_ACCURACY_VALUE',
'Maximum model space distance between geometric entities at asserted c
onnectivities');
#10471=UNCERTAINTY_MEASURE_WITH_UNIT(LENGTH_MEASURE(0.001),#10511,
'DISTANCE_ACCURACY_VALUE',
'Maximum model space distance between geometric entities at asserted c
onnectivities');
#10482=(
GEOMETRIC_REPRESENTATION_CONTEXT(3)
GLOBAL_UNCERTAINTY_ASSIGNED_CONTEXT((#10443))
GLOBAL_UNIT_ASSIGNED_CONTEXT((#10511,#10513,#10514))
REPRESENTATION_CONTEXT('','3D')
);
#10510=(
GEOMETRIC_REPRESENTATION_CONTEXT(3)
GLOBAL_UNCERTAINTY_ASSIGNED_CONTEXT((#10471))
GLOBAL_UNIT_ASSIGNED_CONTEXT((#10511,#10513,#10514))
REPRESENTATION_CONTEXT('','3D')
);
#10511=(
LENGTH_UNIT()
NAMED_UNIT(*)
SI_UNIT(.CENTI.,.METRE.)
);
#10513=(
NAMED_UNIT(*)
PLANE_ANGLE_UNIT()
SI_UNIT($,.RADIAN.)
);
#10514=(
NAMED_UNIT(*)
SI_UNIT($,.STERADIAN.)
SOLID_ANGLE_UNIT()
);
#10525=SHAPE_DEFINITION_REPRESENTATION(#10563,#10655);
#10563=PRODUCT_DEFINITION_SHAPE('',$,#10694);
#10655=SHAPE_REPRESENTATION('',(#5838),#10482);
#10683=PRODUCT_DEFINITION_CONTEXT('part definition',#10799,'design');
#10694=PRODUCT_DEFINITION('M6x18 mounting screw','M6x18 mounting screw',
#10732,#10683);
#10732=PRODUCT_DEFINITION_FORMATION('',$,#10811);
#10799=APPLICATION_CONTEXT(
'Core Data for Automotive Mechanical Design Process');
#10800=PRODUCT_CONTEXT('part definition',#10799,'mechanical');
#10811=PRODUCT('M6x18 mounting screw','M6x18 mounting screw',
'M6x18 mounting screw',(#10800));
#10909=COLOUR_RGB('Black',0.12,0.14,0.17);
#10910=FILL_AREA_STYLE_COLOUR('',#10909);
#10911=FILL_AREA_STYLE('',(#10910));
#10912=SURFACE_STYLE_FILL_AREA(#10911);
#10913=SURFACE_SIDE_STYLE('',(#10912));
#10914=SURFACE_STYLE_USAGE(.BOTH.,#10913);
#10915=PRESENTATION_STYLE_ASSIGNMENT((#10914));
ENDSEC;
END-ISO-10303-21;
